ISO-10303-21;
HEADER;
/* Generated by software containing ST-Developer
 * from STEP Tools, Inc. (www.steptools.com) 
 */

FILE_DESCRIPTION(
/* description */ ('PAT-003'),
/* implementation_level */ '2;1');

FILE_NAME(
/* name */ 'M5x26 bracket screw.step',
/* time_stamp */ '2026-10-29T15:45:40-07:00',
/* author */ (''),
/* organization */ (''),
/* preprocessor_version */ 'ST-DEVELOPER v20.2',
/* originating_system */ 'Autodesk Translation Framework v15.17.0.0',
/* authorisation */ '');

FILE_SCHEMA (('AUTOMOTIVE_DESIGN { 1 0 10303 214 3 1 1 }'));
ENDSEC;

DATA;
#10=MECHANICAL_DESIGN_GEOMETRIC_PRESENTATION_REPRESENTATION('',(#150),#5761);
#105=ORIENTED_CLOSED_SHELL('',*,#3325,.F.);
#107=BREP_WITH_VOIDS('Body1',#3324,(#105));
#110=CONICAL_SURFACE('',#3539,0.4,0.785398163397448);
#111=CONICAL_SURFACE('',#3543,0.41,0.785398163397448);
#112=CONICAL_SURFACE('',#3547,0.26,0.463647609000806);
#126=SHAPE_REPRESENTATION_RELATIONSHIP('SRR','None',#5820,#138);
#138=ADVANCED_BREP_SHAPE_REPRESENTATION('',(#107),#5751);
#150=STYLED_ITEM('',(#5956),#107);
#181=FACE_BOUND('',#575,.T.);
#182=FACE_BOUND('',#583,.T.);
#230=PLANE('',#3531);
#231=PLANE('',#3536);
#232=PLANE('',#3537);
#233=PLANE('',#3545);
#234=PLANE('',#3550);
#235=PLANE('',#3551);
#236=PLANE('',#3552);
#237=PLANE('',#3553);
#238=PLANE('',#3554);
#239=PLANE('',#3555);
#240=PLANE('',#3556);
#241=PLANE('',#3557);
#375=FACE_OUTER_BOUND('',#574,.T.);
#376=FACE_OUTER_BOUND('',#576,.T.);
#377=FACE_OUTER_BOUND('',#577,.T.);
#378=FACE_OUTER_BOUND('',#578,.T.);
#379=FACE_OUTER_BOUND('',#579,.T.);
#380=FACE_OUTER_BOUND('',#580,.T.);
#381=FACE_OUTER_BOUND('',#581,.T.);
#382=FACE_OUTER_BOUND('',#582,.T.);
#383=FACE_OUTER_BOUND('',#584,.T.);
#384=FACE_OUTER_BOUND('',#585,.T.);
#385=FACE_OUTER_BOUND('',#586,.T.);
#386=FACE_OUTER_BOUND('',#587,.T.);
#387=FACE_OUTER_BOUND('',#588,.T.);
#388=FACE_OUTER_BOUND('',#589,.T.);
#389=FACE_OUTER_BOUND('',#590,.T.);
#390=FACE_OUTER_BOUND('',#591,.T.);
#391=FACE_OUTER_BOUND('',#592,.T.);
#392=FACE_OUTER_BOUND('',#593,.T.);
#574=EDGE_LOOP('',(#2372));
#575=EDGE_LOOP('',(#2373));
#576=EDGE_LOOP('',(#2374,#2375,#2376,#2377));
#577=EDGE_LOOP('',(#2378));
#578=EDGE_LOOP('',(#2379));
#579=EDGE_LOOP('',(#2380,#2381,#2382,#2383));
#580=EDGE_LOOP('',(#2384,#2385,#2386,#2387));
#581=EDGE_LOOP('',(#2388,#2389,#2390,#2391));
#582=EDGE_LOOP('',(#2392));
#583=EDGE_LOOP('',(#2393));
#584=EDGE_LOOP('',(#2394,#2395,#2396,#2397));
#585=EDGE_LOOP('',(#2398,#2399,#2400,#2401));
#586=EDGE_LOOP('',(#2402,#2403,#2404,#2405));
#587=EDGE_LOOP('',(#2406,#2407,#2408,#2409));
#588=EDGE_LOOP('',(#2410,#2411,#2412,#2413));
#589=EDGE_LOOP('',(#2414,#2415,#2416,#2417));
#590=EDGE_LOOP('',(#2418,#2419,#2420,#2421));
#591=EDGE_LOOP('',(#2422,#2423,#2424,#2425));
#592=EDGE_LOOP('',(#2426,#2427,#2428,#2429,#2430,#2431));
#593=EDGE_LOOP('',(#2432,#2433,#2434,#2435,#2436,#2437));
#806=LINE('',#4922,#1128);
#807=LINE('',#4931,#1129);
#808=LINE('',#4935,#1130);
#809=LINE('',#4939,#1131);
#810=LINE('',#4946,#1132);
#811=LINE('',#4948,#1133);
#812=LINE('',#4952,#1134);
#813=LINE('',#4954,#1135);
#814=LINE('',#4956,#1136);
#815=LINE('',#4957,#1137);
#816=LINE('',#4960,#1138);
#817=LINE('',#4962,#1139);
#818=LINE('',#4963,#1140);
#819=LINE('',#4966,#1141);
#820=LINE('',#4968,#1142);
#821=LINE('',#4969,#1143);
#822=LINE('',#4972,#1144);
#823=LINE('',#4974,#1145);
#824=LINE('',#4975,#1146);
#825=LINE('',#4978,#1147);
#826=LINE('',#4980,#1148);
#827=LINE('',#4981,#1149);
#828=LINE('',#4983,#1150);
#829=LINE('',#4984,#1151);
#1128=VECTOR('',#3975,0.25);
#1129=VECTOR('',#3988,0.4);
#1130=VECTOR('',#3993,0.425);
#1131=VECTOR('',#3998,0.41);
#1132=VECTOR('',#4007,0.26);
#1133=VECTOR('',#4010,0.25);
#1134=VECTOR('',#4013,1.);
#1135=VECTOR('',#4014,1.);
#1136=VECTOR('',#4015,1.);
#1137=VECTOR('',#4016,1.);
#1138=VECTOR('',#4019,1.);
#1139=VECTOR('',#4020,1.);
#1140=VECTOR('',#4021,1.);
#1141=VECTOR('',#4024,1.);
#1142=VECTOR('',#4025,1.);
#1143=VECTOR('',#4026,1.);
#1144=VECTOR('',#4029,1.);
#1145=VECTOR('',#4030,1.);
#1146=VECTOR('',#4031,1.);
#1147=VECTOR('',#4034,1.);
#1148=VECTOR('',#4035,1.);
#1149=VECTOR('',#4036,1.);
#1150=VECTOR('',#4039,1.);
#1151=VECTOR('',#4040,1.);
#1417=CIRCLE('',#3532,0.25);
#1418=CIRCLE('',#3533,0.24505);
#1419=CIRCLE('',#3535,0.25);
#1420=CIRCLE('',#3538,0.375);
#1421=CIRCLE('',#3540,0.425);
#1422=CIRCLE('',#3542,0.425);
#1423=CIRCLE('',#3544,0.395);
#1424=CIRCLE('',#3546,0.27);
#1425=CIRCLE('',#3548,0.24505);
#1543=VERTEX_POINT('',#4916);
#1544=VERTEX_POINT('',#4918);
#1545=VERTEX_POINT('',#4921);
#1546=VERTEX_POINT('',#4926);
#1547=VERTEX_POINT('',#4929);
#1548=VERTEX_POINT('',#4933);
#1549=VERTEX_POINT('',#4937);
#1550=VERTEX_POINT('',#4941);
#1551=VERTEX_POINT('',#4944);
#1552=VERTEX_POINT('',#4950);
#1553=VERTEX_POINT('',#4951);
#1554=VERTEX_POINT('',#4953);
#1555=VERTEX_POINT('',#4955);
#1556=VERTEX_POINT('',#4959);
#1557=VERTEX_POINT('',#4961);
#1558=VERTEX_POINT('',#4965);
#1559=VERTEX_POINT('',#4967);
#1560=VERTEX_POINT('',#4971);
#1561=VERTEX_POINT('',#4973);
#1562=VERTEX_POINT('',#4977);
#1563=VERTEX_POINT('',#4979);
#1857=EDGE_CURVE('',#1543,#1543,#1417,.T.);
#1858=EDGE_CURVE('',#1544,#1544,#1418,.T.);
#1859=EDGE_CURVE('',#1543,#1545,#806,.T.);
#1860=EDGE_CURVE('',#1545,#1545,#1419,.T.);
#1861=EDGE_CURVE('',#1546,#1546,#1420,.T.);
#1862=EDGE_CURVE('',#1547,#1547,#1421,.T.);
#1863=EDGE_CURVE('',#1547,#1546,#807,.T.);
#1864=EDGE_CURVE('',#1548,#1548,#1422,.T.);
#1865=EDGE_CURVE('',#1548,#1547,#808,.T.);
#1866=EDGE_CURVE('',#1549,#1549,#1423,.T.);
#1867=EDGE_CURVE('',#1549,#1548,#809,.T.);
#1868=EDGE_CURVE('',#1550,#1550,#1424,.T.);
#1869=EDGE_CURVE('',#1551,#1551,#1425,.F.);
#1870=EDGE_CURVE('',#1551,#1550,#810,.T.);
#1871=EDGE_CURVE('',#1544,#1551,#811,.T.);
#1872=EDGE_CURVE('',#1552,#1553,#812,.T.);
#1873=EDGE_CURVE('',#1553,#1554,#813,.T.);
#1874=EDGE_CURVE('',#1554,#1555,#814,.T.);
#1875=EDGE_CURVE('',#1552,#1555,#815,.T.);
#1876=EDGE_CURVE('',#1553,#1556,#816,.T.);
#1877=EDGE_CURVE('',#1556,#1557,#817,.T.);
#1878=EDGE_CURVE('',#1557,#1554,#818,.T.);
#1879=EDGE_CURVE('',#1556,#1558,#819,.T.);
#1880=EDGE_CURVE('',#1558,#1559,#820,.T.);
#1881=EDGE_CURVE('',#1559,#1557,#821,.T.);
#1882=EDGE_CURVE('',#1558,#1560,#822,.T.);
#1883=EDGE_CURVE('',#1560,#1561,#823,.T.);
#1884=EDGE_CURVE('',#1561,#1559,#824,.T.);
#1885=EDGE_CURVE('',#1560,#1562,#825,.T.);
#1886=EDGE_CURVE('',#1562,#1563,#826,.T.);
#1887=EDGE_CURVE('',#1563,#1561,#827,.T.);
#1888=EDGE_CURVE('',#1562,#1552,#828,.T.);
#1889=EDGE_CURVE('',#1555,#1563,#829,.T.);
#2372=ORIENTED_EDGE('',*,*,#1857,.T.);
#2373=ORIENTED_EDGE('',*,*,#1858,.F.);
#2374=ORIENTED_EDGE('',*,*,#1857,.F.);
#2375=ORIENTED_EDGE('',*,*,#1859,.T.);
#2376=ORIENTED_EDGE('',*,*,#1860,.T.);
#2377=ORIENTED_EDGE('',*,*,#1859,.F.);
#2378=ORIENTED_EDGE('',*,*,#1860,.F.);
#2379=ORIENTED_EDGE('',*,*,#1861,.F.);
#2380=ORIENTED_EDGE('',*,*,#1862,.F.);
#2381=ORIENTED_EDGE('',*,*,#1863,.T.);
#2382=ORIENTED_EDGE('',*,*,#1861,.T.);
#2383=ORIENTED_EDGE('',*,*,#1863,.F.);
#2384=ORIENTED_EDGE('',*,*,#1864,.F.);
#2385=ORIENTED_EDGE('',*,*,#1865,.T.);
#2386=ORIENTED_EDGE('',*,*,#1862,.T.);
#2387=ORIENTED_EDGE('',*,*,#1865,.F.);
#2388=ORIENTED_EDGE('',*,*,#1866,.F.);
#2389=ORIENTED_EDGE('',*,*,#1867,.T.);
#2390=ORIENTED_EDGE('',*,*,#1864,.T.);
#2391=ORIENTED_EDGE('',*,*,#1867,.F.);
#2392=ORIENTED_EDGE('',*,*,#1866,.T.);
#2393=ORIENTED_EDGE('',*,*,#1868,.F.);
#2394=ORIENTED_EDGE('',*,*,#1869,.F.);
#2395=ORIENTED_EDGE('',*,*,#1870,.T.);
#2396=ORIENTED_EDGE('',*,*,#1868,.T.);
#2397=ORIENTED_EDGE('',*,*,#1870,.F.);
#2398=ORIENTED_EDGE('',*,*,#1858,.T.);
#2399=ORIENTED_EDGE('',*,*,#1871,.T.);
#2400=ORIENTED_EDGE('',*,*,#1869,.T.);
#2401=ORIENTED_EDGE('',*,*,#1871,.F.);
#2402=ORIENTED_EDGE('',*,*,#1872,.T.);
#2403=ORIENTED_EDGE('',*,*,#1873,.T.);
#2404=ORIENTED_EDGE('',*,*,#1874,.T.);
#2405=ORIENTED_EDGE('',*,*,#1875,.F.);
#2406=ORIENTED_EDGE('',*,*,#1876,.T.);
#2407=ORIENTED_EDGE('',*,*,#1877,.T.);
#2408=ORIENTED_EDGE('',*,*,#1878,.T.);
#2409=ORIENTED_EDGE('',*,*,#1873,.F.);
#2410=ORIENTED_EDGE('',*,*,#1879,.T.);
#2411=ORIENTED_EDGE('',*,*,#1880,.T.);
#2412=ORIENTED_EDGE('',*,*,#1881,.T.);
#2413=ORIENTED_EDGE('',*,*,#1877,.F.);
#2414=ORIENTED_EDGE('',*,*,#1882,.T.);
#2415=ORIENTED_EDGE('',*,*,#1883,.T.);
#2416=ORIENTED_EDGE('',*,*,#1884,.T.);
#2417=ORIENTED_EDGE('',*,*,#1880,.F.);
#2418=ORIENTED_EDGE('',*,*,#1885,.T.);
#2419=ORIENTED_EDGE('',*,*,#1886,.T.);
#2420=ORIENTED_EDGE('',*,*,#1887,.T.);
#2421=ORIENTED_EDGE('',*,*,#1883,.F.);
#2422=ORIENTED_EDGE('',*,*,#1888,.T.);
#2423=ORIENTED_EDGE('',*,*,#1875,.T.);
#2424=ORIENTED_EDGE('',*,*,#1889,.T.);
#2425=ORIENTED_EDGE('',*,*,#1886,.F.);
#2426=ORIENTED_EDGE('',*,*,#1888,.F.);
#2427=ORIENTED_EDGE('',*,*,#1885,.F.);
#2428=ORIENTED_EDGE('',*,*,#1882,.F.);
#2429=ORIENTED_EDGE('',*,*,#1879,.F.);
#2430=ORIENTED_EDGE('',*,*,#1876,.F.);
#2431=ORIENTED_EDGE('',*,*,#1872,.F.);
#2432=ORIENTED_EDGE('',*,*,#1889,.F.);
#2433=ORIENTED_EDGE('',*,*,#1874,.F.);
#2434=ORIENTED_EDGE('',*,*,#1878,.F.);
#2435=ORIENTED_EDGE('',*,*,#1881,.F.);
#2436=ORIENTED_EDGE('',*,*,#1884,.F.);
#2437=ORIENTED_EDGE('',*,*,#1887,.F.);
#3103=CYLINDRICAL_SURFACE('',#3534,0.25);
#3104=CYLINDRICAL_SURFACE('',#3541,0.425);
#3105=CYLINDRICAL_SURFACE('',#3549,0.24505);
#3168=ADVANCED_FACE('',(#375,#181),#230,.T.);
#3169=ADVANCED_FACE('',(#376),#3103,.T.);
#3170=ADVANCED_FACE('',(#377),#231,.F.);
#3171=ADVANCED_FACE('',(#378),#232,.T.);
#3172=ADVANCED_FACE('',(#379),#110,.T.);
#3173=ADVANCED_FACE('',(#380),#3104,.T.);
#3174=ADVANCED_FACE('',(#381),#111,.T.);
#3175=ADVANCED_FACE('',(#382,#182),#233,.T.);
#3176=ADVANCED_FACE('',(#383),#112,.T.);
#3177=ADVANCED_FACE('',(#384),#3105,.T.);
#3178=ADVANCED_FACE('',(#385),#234,.F.);
#3179=ADVANCED_FACE('',(#386),#235,.F.);
#3180=ADVANCED_FACE('',(#387),#236,.F.);
#3181=ADVANCED_FACE('',(#388),#237,.F.);
#3182=ADVANCED_FACE('',(#389),#238,.F.);
#3183=ADVANCED_FACE('',(#390),#239,.F.);
#3184=ADVANCED_FACE('',(#391),#240,.F.);
#3185=ADVANCED_FACE('',(#392),#241,.F.);
#3324=CLOSED_SHELL('',(#3168,#3169,#3170,#3171,#3172,#3173,#3174,#3175,
#3176,#3177));
#3325=CLOSED_SHELL('',(#3178,#3179,#3180,#3181,#3182,#3183,#3184,#3185));
#3530=AXIS2_PLACEMENT_3D('',#4914,#3965,#3966);
#3531=AXIS2_PLACEMENT_3D('',#4915,#3967,#3968);
#3532=AXIS2_PLACEMENT_3D('',#4917,#3969,#3970);
#3533=AXIS2_PLACEMENT_3D('',#4919,#3971,#3972);
#3534=AXIS2_PLACEMENT_3D('',#4920,#3973,#3974);
#3535=AXIS2_PLACEMENT_3D('',#4923,#3976,#3977);
#3536=AXIS2_PLACEMENT_3D('',#4924,#3978,#3979);
#3537=AXIS2_PLACEMENT_3D('',#4925,#3980,#3981);
#3538=AXIS2_PLACEMENT_3D('',#4927,#3982,#3983);
#3539=AXIS2_PLACEMENT_3D('',#4928,#3984,#3985);
#3540=AXIS2_PLACEMENT_3D('',#4930,#3986,#3987);
#3541=AXIS2_PLACEMENT_3D('',#4932,#3989,#3990);
#3542=AXIS2_PLACEMENT_3D('',#4934,#3991,#3992);
#3543=AXIS2_PLACEMENT_3D('',#4936,#3994,#3995);
#3544=AXIS2_PLACEMENT_3D('',#4938,#3996,#3997);
#3545=AXIS2_PLACEMENT_3D('',#4940,#3999,#4000);
#3546=AXIS2_PLACEMENT_3D('',#4942,#4001,#4002);
#3547=AXIS2_PLACEMENT_3D('',#4943,#4003,#4004);
#3548=AXIS2_PLACEMENT_3D('',#4945,#4005,#4006);
#3549=AXIS2_PLACEMENT_3D('',#4947,#4008,#4009);
#3550=AXIS2_PLACEMENT_3D('',#4949,#4011,#4012);
#3551=AXIS2_PLACEMENT_3D('',#4958,#4017,#4018);
#3552=AXIS2_PLACEMENT_3D('',#4964,#4022,#4023);
#3553=AXIS2_PLACEMENT_3D('',#4970,#4027,#4028);
#3554=AXIS2_PLACEMENT_3D('',#4976,#4032,#4033);
#3555=AXIS2_PLACEMENT_3D('',#4982,#4037,#4038);
#3556=AXIS2_PLACEMENT_3D('',#4985,#4041,#4042);
#3557=AXIS2_PLACEMENT_3D('',#4986,#4043,#4044);
#3965=DIRECTION('axis',(0.,0.,1.));
#3966=DIRECTION('refdir',(1.,0.,0.));
#3967=DIRECTION('center_axis',(0.,1.,0.));
#3968=DIRECTION('ref_axis',(1.,0.,0.));
#3969=DIRECTION('center_axis',(0.,1.,0.));
#3970=DIRECTION('ref_axis',(1.,0.,0.));
#3971=DIRECTION('center_axis',(0.,1.,0.));
#3972=DIRECTION('ref_axis',(1.,0.,0.));
#3973=DIRECTION('center_axis',(0.,1.,0.));
#3974=DIRECTION('ref_axis',(1.,0.,0.));
#3975=DIRECTION('',(0.,-1.,0.));
#3976=DIRECTION('center_axis',(0.,1.,0.));
#3977=DIRECTION('ref_axis',(1.,0.,0.));
#3978=DIRECTION('center_axis',(0.,1.,0.));
#3979=DIRECTION('ref_axis',(1.,0.,0.));
#3980=DIRECTION('center_axis',(0.,1.,0.));
#3981=DIRECTION('ref_axis',(0.,0.,1.));
#3982=DIRECTION('center_axis',(0.,-1.,0.));
#3983=DIRECTION('ref_axis',(1.,0.,0.));
#3984=DIRECTION('center_axis',(0.,-1.,0.));
#3985=DIRECTION('ref_axis',(1.,0.,0.));
#3986=DIRECTION('center_axis',(0.,-1.,0.));
#3987=DIRECTION('ref_axis',(1.,0.,0.));
#3988=DIRECTION('',(0.707106781186548,0.707106781186547,8.65956056235493E-17));
#3989=DIRECTION('center_axis',(0.,-1.,0.));
#3990=DIRECTION('ref_axis',(1.,0.,0.));
#3991=DIRECTION('center_axis',(0.,-1.,0.));
#3992=DIRECTION('ref_axis',(1.,0.,0.));
#3993=DIRECTION('',(0.,1.,0.));
#3994=DIRECTION('center_axis',(0.,1.,0.));
#3995=DIRECTION('ref_axis',(1.,0.,0.));
#3996=DIRECTION('center_axis',(0.,-1.,0.));
#3997=DIRECTION('ref_axis',(1.,0.,0.));
#3998=DIRECTION('',(-0.707106781186547,0.707106781186548,-8.65956056235493E-17));
#3999=DIRECTION('center_axis',(0.,-1.,0.));
#4000=DIRECTION('ref_axis',(0.,0.,-1.));
#4001=DIRECTION('center_axis',(0.,-1.,0.));
#4002=DIRECTION('ref_axis',(1.,0.,0.));
#4003=DIRECTION('center_axis',(0.,1.,0.));
#4004=DIRECTION('ref_axis',(1.,0.,0.));
#4005=DIRECTION('center_axis',(0.,1.,0.));
#4006=DIRECTION('ref_axis',(1.,0.,0.));
#4007=DIRECTION('',(-0.447213595499958,0.894427190999916,-5.47678698264203E-17));
#4008=DIRECTION('center_axis',(0.,-1.,0.));
#4009=DIRECTION('ref_axis',(1.,0.,0.));
#4010=DIRECTION('',(0.,1.,0.));
#4011=DIRECTION('center_axis',(0.866025403784439,0.,-0.5));
#4012=DIRECTION('ref_axis',(0.5,0.,0.866025403784439));
#4013=DIRECTION('',(-0.5,0.,-0.866025403784439));
#4014=DIRECTION('',(0.,-1.,0.));
#4015=DIRECTION('',(0.5,0.,0.866025403784439));
#4016=DIRECTION('',(0.,-1.,0.));
#4017=DIRECTION('center_axis',(1.20185167898973E-16,0.,-1.));
#4018=DIRECTION('ref_axis',(1.,0.,1.20185167898973E-16));
#4019=DIRECTION('',(-1.,0.,-1.20185167898973E-16));
#4020=DIRECTION('',(0.,-1.,0.));
#4021=DIRECTION('',(1.,0.,1.20185167898973E-16));
#4022=DIRECTION('center_axis',(-0.866025403784439,0.,-0.5));
#4023=DIRECTION('ref_axis',(0.5,0.,-0.866025403784439));
#4024=DIRECTION('',(-0.5,0.,0.866025403784439));
#4025=DIRECTION('',(0.,-1.,0.));
#4026=DIRECTION('',(0.5,0.,-0.866025403784439));
#4027=DIRECTION('center_axis',(-0.866025403784439,0.,0.5));
#4028=DIRECTION('ref_axis',(-0.5,0.,-0.866025403784439));
#4029=DIRECTION('',(0.5,0.,0.866025403784439));
#4030=DIRECTION('',(0.,-1.,0.));
#4031=DIRECTION('',(-0.5,0.,-0.866025403784439));
#4032=DIRECTION('center_axis',(-2.40370335797945E-16,0.,1.));
#4033=DIRECTION('ref_axis',(-1.,0.,-2.40370335797945E-16));
#4034=DIRECTION('',(1.,0.,2.40370335797945E-16));
#4035=DIRECTION('',(0.,-1.,0.));
#4036=DIRECTION('',(-1.,0.,-2.40370335797945E-16));
#4037=DIRECTION('center_axis',(0.866025403784439,0.,0.5));
#4038=DIRECTION('ref_axis',(-0.5,0.,0.866025403784439));
#4039=DIRECTION('',(0.5,0.,-0.866025403784439));
#4040=DIRECTION('',(-0.5,0.,0.866025403784439));
#4041=DIRECTION('center_axis',(0.,1.,0.));
#4042=DIRECTION('ref_axis',(1.,0.,0.));
#4043=DIRECTION('center_axis',(0.,-1.,0.));
#4044=DIRECTION('ref_axis',(0.,0.,-1.));
#4914=CARTESIAN_POINT('',(0.,0.,0.));
#4915=CARTESIAN_POINT('Origin',(0.,-1.39,0.));
#4916=CARTESIAN_POINT('',(-0.25,-1.39,3.06161699786838E-17));
#4917=CARTESIAN_POINT('Origin',(0.,-1.39,0.));
#4918=CARTESIAN_POINT('',(-0.24505,-1.39,3.00099698131059E-17));
#4919=CARTESIAN_POINT('Origin',(0.,-1.39,0.));
#4920=CARTESIAN_POINT('Origin',(0.,-2.6,0.));
#4921=CARTESIAN_POINT('',(-0.25,-2.6,3.06161699786838E-17));
#4922=CARTESIAN_POINT('',(-0.25,-2.6,3.06161699786838E-17));
#4923=CARTESIAN_POINT('Origin',(0.,-2.6,0.));
#4924=CARTESIAN_POINT('Origin',(0.,-2.6,0.));
#4925=CARTESIAN_POINT('Origin',(0.375,0.5,0.));
#4926=CARTESIAN_POINT('',(-0.375,0.5,-4.59242549680257E-17));
#4927=CARTESIAN_POINT('Origin',(0.,0.5,0.));
#4928=CARTESIAN_POINT('Origin',(0.,0.475,0.));
#4929=CARTESIAN_POINT('',(-0.425,0.45,-5.20474889637625E-17));
#4930=CARTESIAN_POINT('Origin',(0.,0.45,0.));
#4931=CARTESIAN_POINT('',(-0.4,0.475,-4.89858719658941E-17));
#4932=CARTESIAN_POINT('Origin',(0.,0.24,0.));
#4933=CARTESIAN_POINT('',(-0.425,0.0299999999999998,-5.20474889637625E-17));
#4934=CARTESIAN_POINT('Origin',(0.,0.0299999999999998,0.));
#4935=CARTESIAN_POINT('',(-0.425,0.24,-5.20474889637625E-17));
#4936=CARTESIAN_POINT('Origin',(0.,0.0150000000000001,0.));
#4937=CARTESIAN_POINT('',(-0.395,4.85722573273506E-17,-4.83735485663204E-17));
#4938=CARTESIAN_POINT('Origin',(0.,0.,0.));
#4939=CARTESIAN_POINT('',(-0.41,0.0150000000000001,-5.02105187650415E-17));
#4940=CARTESIAN_POINT('Origin',(0.27,0.,0.));
#4941=CARTESIAN_POINT('',(-0.27,0.,-3.30654635769785E-17));
#4942=CARTESIAN_POINT('Origin',(0.,0.,0.));
#4943=CARTESIAN_POINT('Origin',(0.,-0.02,0.));
#4944=CARTESIAN_POINT('',(-0.24505,-0.0498999999999999,3.00099698131059E-17));
#4945=CARTESIAN_POINT('Origin',(0.,-0.0498999999999999,0.));
#4946=CARTESIAN_POINT('',(-0.26,-0.02,-3.18408167778312E-17));
#4947=CARTESIAN_POINT('Origin',(0.,-0.995,0.));
#4948=CARTESIAN_POINT('',(-0.24505,-0.995,-3.00099698131059E-17));
#4949=CARTESIAN_POINT('Origin',(0.115470053837925,-0.5,-0.2));
#4950=CARTESIAN_POINT('',(0.23094010767585,-0.5,0.));
#4951=CARTESIAN_POINT('',(0.115470053837925,-0.5,-0.2));
#4952=CARTESIAN_POINT('',(0.23094010767585,-0.5,0.));
#4953=CARTESIAN_POINT('',(0.115470053837925,-0.8,-0.2));
#4954=CARTESIAN_POINT('',(0.115470053837925,-0.5,-0.2));
#4955=CARTESIAN_POINT('',(0.23094010767585,-0.8,0.));
#4956=CARTESIAN_POINT('',(0.23094010767585,-0.8,0.));
#4957=CARTESIAN_POINT('',(0.23094010767585,-0.5,0.));
#4958=CARTESIAN_POINT('Origin',(-0.115470053837925,-0.5,-0.2));
#4959=CARTESIAN_POINT('',(-0.115470053837925,-0.5,-0.2));
#4960=CARTESIAN_POINT('',(0.115470053837925,-0.5,-0.2));
#4961=CARTESIAN_POINT('',(-0.115470053837925,-0.8,-0.2));
#4962=CARTESIAN_POINT('',(-0.115470053837925,-0.5,-0.2));
#4963=CARTESIAN_POINT('',(0.115470053837925,-0.8,-0.2));
#4964=CARTESIAN_POINT('Origin',(-0.23094010767585,-0.5,-2.77555756156289E-17));
#4965=CARTESIAN_POINT('',(-0.23094010767585,-0.5,-2.82820063659975E-17));
#4966=CARTESIAN_POINT('',(-0.115470053837925,-0.5,-0.2));
#4967=CARTESIAN_POINT('',(-0.23094010767585,-0.8,-2.77555756156289E-17));
#4968=CARTESIAN_POINT('',(-0.23094010767585,-0.5,-2.82820063659975E-17));
#4969=CARTESIAN_POINT('',(-0.115470053837925,-0.8,-0.2));
#4970=CARTESIAN_POINT('Origin',(-0.115470053837925,-0.5,0.2));
#4971=CARTESIAN_POINT('',(-0.115470053837925,-0.5,0.2));
#4972=CARTESIAN_POINT('',(-0.23094010767585,-0.5,-2.82820063659975E-17));
#4973=CARTESIAN_POINT('',(-0.115470053837925,-0.8,0.2));
#4974=CARTESIAN_POINT('',(-0.115470053837925,-0.5,0.2));
#4975=CARTESIAN_POINT('',(-0.23094010767585,-0.8,-2.82820063659975E-17));
#4976=CARTESIAN_POINT('Origin',(0.115470053837925,-0.5,0.2));
#4977=CARTESIAN_POINT('',(0.115470053837925,-0.5,0.2));
#4978=CARTESIAN_POINT('',(-0.115470053837925,-0.5,0.2));
#4979=CARTESIAN_POINT('',(0.115470053837925,-0.8,0.2));
#4980=CARTESIAN_POINT('',(0.115470053837925,-0.5,0.2));
#4981=CARTESIAN_POINT('',(-0.115470053837925,-0.8,0.2));
#4982=CARTESIAN_POINT('Origin',(0.23094010767585,-0.5,0.));
#4983=CARTESIAN_POINT('',(0.115470053837925,-0.5,0.2));
#4984=CARTESIAN_POINT('',(0.115470053837925,-0.8,0.2));
#4985=CARTESIAN_POINT('Origin',(0.,-0.5,0.));
#4986=CARTESIAN_POINT('Origin',(0.,-0.8,0.));
#5735=UNCERTAINTY_MEASURE_WITH_UNIT(LENGTH_MEASURE(0.001),#5762,
'DISTANCE_ACCURACY_VALUE',
'Maximum model space distance between geometric entities at asserted c
onnectivities');
#5745=UNCERTAINTY_MEASURE_WITH_UNIT(LENGTH_MEASURE(0.001),#5762,
'DISTANCE_ACCURACY_VALUE',
'Maximum model space distance between geometric entities at asserted c
onnectivities');
#5751=(
GEOMETRIC_REPRESENTATION_CONTEXT(3)
GLOBAL_UNCERTAINTY_ASSIGNED_CONTEXT((#5735))
GLOBAL_UNIT_ASSIGNED_CONTEXT((#5762,#5764,#5765))
REPRESENTATION_CONTEXT('','3D')
);
#5761=(
GEOMETRIC_REPRESENTATION_CONTEXT(3)
GLOBAL_UNCERTAINTY_ASSIGNED_CONTEXT((#5745))
GLOBAL_UNIT_ASSIGNED_CONTEXT((#5762,#5764,#5765))
REPRESENTATION_CONTEXT('','3D')
);
#5762=(
LENGTH_UNIT()
NAMED_UNIT(*)
SI_UNIT(.CENTI.,.METRE.)
);
#5764=(
NAMED_UNIT(*)
PLANE_ANGLE_UNIT()
SI_UNIT($,.RADIAN.)
);
#5765=(
NAMED_UNIT(*)
SI_UNIT($,.STERADIAN.)
SOLID_ANGLE_UNIT()
);
#5771=SHAPE_DEFINITION_REPRESENTATION(#5786,#5820);
#5786=PRODUCT_DEFINITION_SHAPE('',$,#5836);
#5820=SHAPE_REPRESENTATION('',(#3530),#5751);
#5830=PRODUCT_DEFINITION_CONTEXT('part definition',#5877,'design');
#5836=PRODUCT_DEFINITION('M5x26 bracket screw','M5x26 bracket screw',#5851,
#5830);
#5851=PRODUCT_DEFINITION_FORMATION('',$,#5884);
#5877=APPLICATION_CONTEXT(
'Core Data for Automotive Mechanical Design Process');
#5878=PRODUCT_CONTEXT('part definition',#5877,'mechanical');
#5884=PRODUCT('M5x26 bracket screw','M5x26 bracket screw',
'M5x26 bracket screw',(#5878));
#5950=COLOUR_RGB('Black',0.12,0.14,0.17);
#5951=FILL_AREA_STYLE_COLOUR('',#5950);
#5952=FILL_AREA_STYLE('',(#5951));
#5953=SURFACE_STYLE_FILL_AREA(#5952);
#5954=SURFACE_SIDE_STYLE('',(#5953));
#5955=SURFACE_STYLE_USAGE(.BOTH.,#5954);
#5956=PRESENTATION_STYLE_ASSIGNMENT((#5955));
ENDSEC;
END-ISO-10303-21;
